ISO-10303-21;
HEADER;
/* Generated by software containing ST-Developer
 * from STEP Tools, Inc. (www.steptools.com) 
 */

FILE_DESCRIPTION(
/* description */ ('Chute with adjustable gate'),
/* implementation_level */ '2;1');

FILE_NAME(
/* name */ 'Flat Washer - M5.step',
/* time_stamp */ '2026-10-27T10:52:28-07:00',
/* author */ (''),
/* organization */ (''),
/* preprocessor_version */ 'ST-DEVELOPER v20.2',
/* originating_system */ 'Autodesk Translation Framework v15.17.0.0',
/* authorisation */ '');

FILE_SCHEMA (('AUTOMOTIVE_DESIGN { 1 0 10303 214 3 1 1 }'));
ENDSEC;

DATA;
#10=MECHANICAL_DESIGN_GEOMETRIC_PRESENTATION_REPRESENTATION('',(#437),#13094);
#335=CONICAL_SURFACE('',#8412,0.275,0.785398163397449);
#373=SHAPE_REPRESENTATION_RELATIONSHIP('SRR','None',#13274,#405);
#405=ADVANCED_BREP_SHAPE_REPRESENTATION('',(#468),#13083);
#437=STYLED_ITEM('',(#13502),#468);
#468=MANIFOLD_SOLID_BREP('Body1',#7621);
#566=FACE_BOUND('',#1712,.T.);
#567=FACE_BOUND('',#1715,.T.);
#822=PLANE('',#8417);
#823=PLANE('',#8421);
#1202=FACE_OUTER_BOUND('',#1709,.T.);
#1203=FACE_OUTER_BOUND('',#1710,.T.);
#1204=FACE_OUTER_BOUND('',#1711,.T.);
#1205=FACE_OUTER_BOUND('',#1713,.T.);
#1206=FACE_OUTER_BOUND('',#1714,.T.);
#1709=EDGE_LOOP('',(#6534,#6535,#6536,#6537));
#1710=EDGE_LOOP('',(#6538,#6539,#6540,#6541));
#1711=EDGE_LOOP('',(#6542));
#1712=EDGE_LOOP('',(#6543));
#1713=EDGE_LOOP('',(#6544,#6545,#6546,#6547));
#1714=EDGE_LOOP('',(#6548));
#1715=EDGE_LOOP('',(#6549));
#2422=LINE('',#12339,#3199);
#2423=LINE('',#12343,#3200);
#2424=LINE('',#12350,#3201);
#3199=VECTOR('',#10116,0.275);
#3200=VECTOR('',#10121,0.265);
#3201=VECTOR('',#10130,0.5);
#3524=CIRCLE('',#8413,0.285);
#3525=CIRCLE('',#8414,0.265);
#3526=CIRCLE('',#8416,0.265);
#3527=CIRCLE('',#8418,0.5);
#3528=CIRCLE('',#8420,0.5);
#4041=VERTEX_POINT('',#12336);
#4042=VERTEX_POINT('',#12338);
#4043=VERTEX_POINT('',#12342);
#4044=VERTEX_POINT('',#12346);
#4045=VERTEX_POINT('',#12349);
#4900=EDGE_CURVE('',#4041,#4041,#3524,.T.);
#4901=EDGE_CURVE('',#4041,#4042,#2422,.T.);
#4902=EDGE_CURVE('',#4042,#4042,#3525,.T.);
#4903=EDGE_CURVE('',#4042,#4043,#2423,.T.);
#4904=EDGE_CURVE('',#4043,#4043,#3526,.T.);
#4905=EDGE_CURVE('',#4044,#4044,#3527,.T.);
#4906=EDGE_CURVE('',#4044,#4045,#2424,.T.);
#4907=EDGE_CURVE('',#4045,#4045,#3528,.T.);
#6534=ORIENTED_EDGE('',*,*,#4900,.T.);
#6535=ORIENTED_EDGE('',*,*,#4901,.T.);
#6536=ORIENTED_EDGE('',*,*,#4902,.T.);
#6537=ORIENTED_EDGE('',*,*,#4901,.F.);
#6538=ORIENTED_EDGE('',*,*,#4902,.F.);
#6539=ORIENTED_EDGE('',*,*,#4903,.T.);
#6540=ORIENTED_EDGE('',*,*,#4904,.T.);
#6541=ORIENTED_EDGE('',*,*,#4903,.F.);
#6542=ORIENTED_EDGE('',*,*,#4905,.T.);
#6543=ORIENTED_EDGE('',*,*,#4900,.F.);
#6544=ORIENTED_EDGE('',*,*,#4905,.F.);
#6545=ORIENTED_EDGE('',*,*,#4906,.T.);
#6546=ORIENTED_EDGE('',*,*,#4907,.T.);
#6547=ORIENTED_EDGE('',*,*,#4906,.F.);
#6548=ORIENTED_EDGE('',*,*,#4907,.F.);
#6549=ORIENTED_EDGE('',*,*,#4904,.F.);
#7158=CYLINDRICAL_SURFACE('',#8415,0.265);
#7159=CYLINDRICAL_SURFACE('',#8419,0.5);
#7470=ADVANCED_FACE('',(#1202),#335,.F.);
#7471=ADVANCED_FACE('',(#1203),#7158,.F.);
#7472=ADVANCED_FACE('',(#1204,#566),#822,.T.);
#7473=ADVANCED_FACE('',(#1205),#7159,.T.);
#7474=ADVANCED_FACE('',(#1206,#567),#823,.F.);
#7621=CLOSED_SHELL('',(#7470,#7471,#7472,#7473,#7474));
#8411=AXIS2_PLACEMENT_3D('',#12334,#10110,#10111);
#8412=AXIS2_PLACEMENT_3D('',#12335,#10112,#10113);
#8413=AXIS2_PLACEMENT_3D('',#12337,#10114,#10115);
#8414=AXIS2_PLACEMENT_3D('',#12340,#10117,#10118);
#8415=AXIS2_PLACEMENT_3D('',#12341,#10119,#10120);
#8416=AXIS2_PLACEMENT_3D('',#12344,#10122,#10123);
#8417=AXIS2_PLACEMENT_3D('',#12345,#10124,#10125);
#8418=AXIS2_PLACEMENT_3D('',#12347,#10126,#10127);
#8419=AXIS2_PLACEMENT_3D('',#12348,#10128,#10129);
#8420=AXIS2_PLACEMENT_3D('',#12351,#10131,#10132);
#8421=AXIS2_PLACEMENT_3D('',#12352,#10133,#10134);
#10110=DIRECTION('axis',(0.,0.,1.));
#10111=DIRECTION('refdir',(1.,0.,0.));
#10112=DIRECTION('center_axis',(0.,1.,0.));
#10113=DIRECTION('ref_axis',(1.,0.,0.));
#10114=DIRECTION('center_axis',(0.,1.,0.));
#10115=DIRECTION('ref_axis',(1.,0.,0.));
#10116=DIRECTION('',(0.707106781186548,-0.707106781186547,-8.65956056235494E-17));
#10117=DIRECTION('center_axis',(0.,-1.,0.));
#10118=DIRECTION('ref_axis',(1.,0.,0.));
#10119=DIRECTION('center_axis',(0.,1.,0.));
#10120=DIRECTION('ref_axis',(1.,0.,0.));
#10121=DIRECTION('',(0.,-1.,0.));
#10122=DIRECTION('center_axis',(0.,-1.,0.));
#10123=DIRECTION('ref_axis',(1.,0.,0.));
#10124=DIRECTION('center_axis',(0.,1.,0.));
#10125=DIRECTION('ref_axis',(1.,0.,0.));
#10126=DIRECTION('center_axis',(0.,1.,0.));
#10127=DIRECTION('ref_axis',(1.,0.,0.));
#10128=DIRECTION('center_axis',(0.,1.,0.));
#10129=DIRECTION('ref_axis',(1.,0.,0.));
#10130=DIRECTION('',(0.,-1.,0.));
#10131=DIRECTION('center_axis',(0.,1.,0.));
#10132=DIRECTION('ref_axis',(1.,0.,0.));
#10133=DIRECTION('center_axis',(0.,1.,0.));
#10134=DIRECTION('ref_axis',(1.,0.,0.));
#12334=CARTESIAN_POINT('',(0.,0.,0.));
#12335=CARTESIAN_POINT('Origin',(0.,0.09,0.));
#12336=CARTESIAN_POINT('',(-0.285,0.1,3.49024337756996E-17));
#12337=CARTESIAN_POINT('Origin',(0.,0.1,0.));
#12338=CARTESIAN_POINT('',(-0.265,0.08,-3.24531401774049E-17));
#12339=CARTESIAN_POINT('',(-0.275,0.09,3.36777869765522E-17));
#12340=CARTESIAN_POINT('Origin',(0.,0.08,0.));
#12341=CARTESIAN_POINT('Origin',(0.,0.,0.));
#12342=CARTESIAN_POINT('',(-0.265,0.,3.24531401774049E-17));
#12343=CARTESIAN_POINT('',(-0.265,0.,3.24531401774049E-17));
#12344=CARTESIAN_POINT('Origin',(0.,0.,0.));
#12345=CARTESIAN_POINT('Origin',(0.,0.1,0.));
#12346=CARTESIAN_POINT('',(-0.5,0.1,6.12323399573677E-17));
#12347=CARTESIAN_POINT('Origin',(0.,0.1,0.));
#12348=CARTESIAN_POINT('Origin',(0.,0.,0.));
#12349=CARTESIAN_POINT('',(-0.5,0.,6.12323399573677E-17));
#12350=CARTESIAN_POINT('',(-0.5,0.,6.12323399573677E-17));
#12351=CARTESIAN_POINT('Origin',(0.,0.,0.));
#12352=CARTESIAN_POINT('Origin',(0.,0.,0.));
#13046=UNCERTAINTY_MEASURE_WITH_UNIT(LENGTH_MEASURE(0.001),#13095,
'DISTANCE_ACCURACY_VALUE',
'Maximum model space distance between geometric entities at asserted c
onnectivities');
#13057=UNCERTAINTY_MEASURE_WITH_UNIT(LENGTH_MEASURE(0.001),#13095,
'DISTANCE_ACCURACY_VALUE',
'Maximum model space distance between geometric entities at asserted c
onnectivities');
#13083=(
GEOMETRIC_REPRESENTATION_CONTEXT(3)
GLOBAL_UNCERTAINTY_ASSIGNED_CONTEXT((#13046))
GLOBAL_UNIT_ASSIGNED_CONTEXT((#13095,#13097,#13098))
REPRESENTATION_CONTEXT('','3D')
);
#13094=(
GEOMETRIC_REPRESENTATION_CONTEXT(3)
GLOBAL_UNCERTAINTY_ASSIGNED_CONTEXT((#13057))
GLOBAL_UNIT_ASSIGNED_CONTEXT((#13095,#13097,#13098))
REPRESENTATION_CONTEXT('','3D')
);
#13095=(
LENGTH_UNIT()
NAMED_UNIT(*)
SI_UNIT(.CENTI.,.METRE.)
);
#13097=(
NAMED_UNIT(*)
PLANE_ANGLE_UNIT()
SI_UNIT($,.RADIAN.)
);
#13098=(
NAMED_UNIT(*)
SI_UNIT($,.STERADIAN.)
SOLID_ANGLE_UNIT()
);
#13124=SHAPE_DEFINITION_REPRESENTATION(#13160,#13274);
#13160=PRODUCT_DEFINITION_SHAPE('',$,#13311);
#13274=SHAPE_REPRESENTATION('',(#8411),#13083);
#13285=PRODUCT_DEFINITION_CONTEXT('part definition',#13395,'design');
#13311=PRODUCT_DEFINITION('Flat Washer - M5','Flat Washer - M5',#13347,
#13285);
#13347=PRODUCT_DEFINITION_FORMATION('',$,#13422);
#13395=APPLICATION_CONTEXT(
'Core Data for Automotive Mechanical Design Process');
#13396=PRODUCT_CONTEXT('part definition',#13395,'mechanical');
#13422=PRODUCT('Flat Washer - M5','Flat Washer - M5','Flat Washer - M5',
(#13396));
#13496=COLOUR_RGB('Black',0.12,0.14,0.17);
#13497=FILL_AREA_STYLE_COLOUR('',#13496);
#13498=FILL_AREA_STYLE('',(#13497));
#13499=SURFACE_STYLE_FILL_AREA(#13498);
#13500=SURFACE_SIDE_STYLE('',(#13499));
#13501=SURFACE_STYLE_USAGE(.BOTH.,#13500);
#13502=PRESENTATION_STYLE_ASSIGNMENT((#13501));
ENDSEC;
END-ISO-10303-21;
